ISO-10303-21;
HEADER;
/* Generated by software containing ST-Developer
 * from STEP Tools, Inc. (www.steptools.com) 
 */

FILE_DESCRIPTION(
/* description */ ('PAT-072'),
/* implementation_level */ '2;1');

FILE_NAME(
/* name */ 'Body.step',
/* time_stamp */ '2026-10-29T20:11:56-07:00',
/* author */ (''),
/* organization */ (''),
/* preprocessor_version */ 'ST-DEVELOPER v20.2',
/* originating_system */ 'Autodesk Translation Framework v15.17.0.0',
/* authorisation */ '');

FILE_SCHEMA (('AUTOMOTIVE_DESIGN { 1 0 10303 214 3 1 1 }'));
ENDSEC;

DATA;
#10=MECHANICAL_DESIGN_GEOMETRIC_PRESENTATION_REPRESENTATION('',(#364),#11432);
#292=SHAPE_REPRESENTATION_RELATIONSHIP('SRR','None',#11597,#328);
#328=ADVANCED_BREP_SHAPE_REPRESENTATION('',(#399),#11428);
#364=STYLED_ITEM('',(#11798),#399);
#399=MANIFOLD_SOLID_BREP('Body1',#6100);
#556=FACE_BOUND('',#1641,.T.);
#557=FACE_BOUND('',#1643,.T.);
#558=FACE_BOUND('',#1645,.T.);
#559=FACE_BOUND('',#1653,.T.);
#560=FACE_BOUND('',#1656,.T.);
#561=FACE_BOUND('',#1660,.T.);
#760=PLANE('',#7122);
#761=PLANE('',#7124);
#762=PLANE('',#7126);
#763=PLANE('',#7128);
#764=PLANE('',#7129);
#765=PLANE('',#7130);
#766=PLANE('',#7131);
#767=PLANE('',#7132);
#768=PLANE('',#7133);
#769=PLANE('',#7134);
#770=PLANE('',#7138);
#771=PLANE('',#7143);
#1113=FACE_OUTER_BOUND('',#1639,.T.);
#1114=FACE_OUTER_BOUND('',#1640,.T.);
#1115=FACE_OUTER_BOUND('',#1642,.T.);
#1116=FACE_OUTER_BOUND('',#1644,.T.);
#1117=FACE_OUTER_BOUND('',#1646,.T.);
#1118=FACE_OUTER_BOUND('',#1647,.T.);
#1119=FACE_OUTER_BOUND('',#1648,.T.);
#1120=FACE_OUTER_BOUND('',#1649,.T.);
#1121=FACE_OUTER_BOUND('',#1650,.T.);
#1122=FACE_OUTER_BOUND('',#1651,.T.);
#1123=FACE_OUTER_BOUND('',#1652,.T.);
#1124=FACE_OUTER_BOUND('',#1654,.T.);
#1125=FACE_OUTER_BOUND('',#1655,.T.);
#1126=FACE_OUTER_BOUND('',#1657,.T.);
#1127=FACE_OUTER_BOUND('',#1658,.T.);
#1128=FACE_OUTER_BOUND('',#1659,.T.);
#1129=FACE_OUTER_BOUND('',#1661,.T.);
#1639=EDGE_LOOP('',(#5348,#5349,#5350,#5351));
#1640=EDGE_LOOP('',(#5352));
#1641=EDGE_LOOP('',(#5353));
#1642=EDGE_LOOP('',(#5354,#5355,#5356,#5357,#5358,#5359));
#1643=EDGE_LOOP('',(#5360));
#1644=EDGE_LOOP('',(#5361,#5362,#5363,#5364,#5365,#5366));
#1645=EDGE_LOOP('',(#5367));
#1646=EDGE_LOOP('',(#5368,#5369,#5370,#5371));
#1647=EDGE_LOOP('',(#5372,#5373,#5374,#5375));
#1648=EDGE_LOOP('',(#5376,#5377,#5378,#5379));
#1649=EDGE_LOOP('',(#5380,#5381,#5382,#5383));
#1650=EDGE_LOOP('',(#5384,#5385,#5386,#5387));
#1651=EDGE_LOOP('',(#5388,#5389,#5390,#5391));
#1652=EDGE_LOOP('',(#5392));
#1653=EDGE_LOOP('',(#5393));
#1654=EDGE_LOOP('',(#5394,#5395,#5396,#5397));
#1655=EDGE_LOOP('',(#5398));
#1656=EDGE_LOOP('',(#5399));
#1657=EDGE_LOOP('',(#5400,#5401,#5402,#5403));
#1658=EDGE_LOOP('',(#5404,#5405,#5406,#5407));
#1659=EDGE_LOOP('',(#5408));
#1660=EDGE_LOOP('',(#5409));
#1661=EDGE_LOOP('',(#5410,#5411,#5412,#5413));
#2054=LINE('',#11078,#2473);
#2055=LINE('',#11086,#2474);
#2056=LINE('',#11088,#2475);
#2057=LINE('',#11090,#2476);
#2058=LINE('',#11092,#2477);
#2059=LINE('',#11094,#2478);
#2060=LINE('',#11095,#2479);
#2061=LINE('',#11101,#2480);
#2062=LINE('',#11103,#2481);
#2063=LINE('',#11105,#2482);
#2064=LINE('',#11107,#2483);
#2065=LINE('',#11109,#2484);
#2066=LINE('',#11110,#2485);
#2067=LINE('',#11114,#2486);
#2068=LINE('',#11115,#2487);
#2069=LINE('',#11117,#2488);
#2070=LINE('',#11119,#2489);
#2071=LINE('',#11121,#2490);
#2072=LINE('',#11123,#2491);
#2073=LINE('',#11130,#2492);
#2074=LINE('',#11136,#2493);
#2075=LINE('',#11140,#2494);
#2076=LINE('',#11145,#2495);
#2473=VECTOR('',#8843,0.43);
#2474=VECTOR('',#8852,1.);
#2475=VECTOR('',#8853,1.);
#2476=VECTOR('',#8854,1.);
#2477=VECTOR('',#8855,1.);
#2478=VECTOR('',#8856,1.);
#2479=VECTOR('',#8857,1.);
#2480=VECTOR('',#8862,1.);
#2481=VECTOR('',#8863,1.);
#2482=VECTOR('',#8864,1.);
#2483=VECTOR('',#8865,1.);
#2484=VECTOR('',#8866,1.);
#2485=VECTOR('',#8867,1.);
#2486=VECTOR('',#8872,1.);
#2487=VECTOR('',#8873,1.);
#2488=VECTOR('',#8876,1.);
#2489=VECTOR('',#8879,1.);
#2490=VECTOR('',#8882,1.);
#2491=VECTOR('',#8885,1.);
#2492=VECTOR('',#8894,0.46);
#2493=VECTOR('',#8903,0.525);
#2494=VECTOR('',#8908,0.515);
#2495=VECTOR('',#8915,0.2);
#2804=CIRCLE('',#7120,0.43);
#2805=CIRCLE('',#7121,0.43);
#2806=CIRCLE('',#7123,0.2);
#2807=CIRCLE('',#7125,0.525);
#2808=CIRCLE('',#7127,0.515);
#2809=CIRCLE('',#7135,0.46);
#2810=CIRCLE('',#7137,0.46);
#2811=CIRCLE('',#7139,0.525);
#2812=CIRCLE('',#7142,0.515);
#2813=CIRCLE('',#7144,0.2);
#3255=VERTEX_POINT('',#11075);
#3256=VERTEX_POINT('',#11077);
#3257=VERTEX_POINT('',#11081);
#3258=VERTEX_POINT('',#11084);
#3259=VERTEX_POINT('',#11085);
#3260=VERTEX_POINT('',#11087);
#3261=VERTEX_POINT('',#11089);
#3262=VERTEX_POINT('',#11091);
#3263=VERTEX_POINT('',#11093);
#3264=VERTEX_POINT('',#11096);
#3265=VERTEX_POINT('',#11099);
#3266=VERTEX_POINT('',#11100);
#3267=VERTEX_POINT('',#11102);
#3268=VERTEX_POINT('',#11104);
#3269=VERTEX_POINT('',#11106);
#3270=VERTEX_POINT('',#11108);
#3271=VERTEX_POINT('',#11111);
#3272=VERTEX_POINT('',#11126);
#3273=VERTEX_POINT('',#11129);
#3274=VERTEX_POINT('',#11133);
#3275=VERTEX_POINT('',#11138);
#3276=VERTEX_POINT('',#11142);
#3963=EDGE_CURVE('',#3255,#3255,#2804,.T.);
#3964=EDGE_CURVE('',#3255,#3256,#2054,.T.);
#3965=EDGE_CURVE('',#3256,#3256,#2805,.T.);
#3966=EDGE_CURVE('',#3257,#3257,#2806,.T.);
#3967=EDGE_CURVE('',#3258,#3259,#2055,.T.);
#3968=EDGE_CURVE('',#3259,#3260,#2056,.T.);
#3969=EDGE_CURVE('',#3260,#3261,#2057,.T.);
#3970=EDGE_CURVE('',#3261,#3262,#2058,.T.);
#3971=EDGE_CURVE('',#3262,#3263,#2059,.T.);
#3972=EDGE_CURVE('',#3263,#3258,#2060,.T.);
#3973=EDGE_CURVE('',#3264,#3264,#2807,.T.);
#3974=EDGE_CURVE('',#3265,#3266,#2061,.T.);
#3975=EDGE_CURVE('',#3267,#3265,#2062,.T.);
#3976=EDGE_CURVE('',#3268,#3267,#2063,.T.);
#3977=EDGE_CURVE('',#3269,#3268,#2064,.T.);
#3978=EDGE_CURVE('',#3270,#3269,#2065,.T.);
#3979=EDGE_CURVE('',#3266,#3270,#2066,.T.);
#3980=EDGE_CURVE('',#3271,#3271,#2808,.T.);
#3981=EDGE_CURVE('',#3265,#3258,#2067,.T.);
#3982=EDGE_CURVE('',#3267,#3263,#2068,.T.);
#3983=EDGE_CURVE('',#3268,#3262,#2069,.T.);
#3984=EDGE_CURVE('',#3269,#3261,#2070,.T.);
#3985=EDGE_CURVE('',#3270,#3260,#2071,.T.);
#3986=EDGE_CURVE('',#3266,#3259,#2072,.T.);
#3987=EDGE_CURVE('',#3272,#3272,#2809,.T.);
#3988=EDGE_CURVE('',#3272,#3273,#2073,.T.);
#3989=EDGE_CURVE('',#3273,#3273,#2810,.T.);
#3990=EDGE_CURVE('',#3274,#3274,#2811,.T.);
#3991=EDGE_CURVE('',#3264,#3274,#2074,.T.);
#3992=EDGE_CURVE('',#3275,#3275,#2812,.T.);
#3993=EDGE_CURVE('',#3275,#3271,#2075,.T.);
#3994=EDGE_CURVE('',#3276,#3276,#2813,.T.);
#3995=EDGE_CURVE('',#3276,#3257,#2076,.T.);
#5348=ORIENTED_EDGE('',*,*,#3963,.F.);
#5349=ORIENTED_EDGE('',*,*,#3964,.T.);
#5350=ORIENTED_EDGE('',*,*,#3965,.F.);
#5351=ORIENTED_EDGE('',*,*,#3964,.F.);
#5352=ORIENTED_EDGE('',*,*,#3963,.T.);
#5353=ORIENTED_EDGE('',*,*,#3966,.F.);
#5354=ORIENTED_EDGE('',*,*,#3967,.T.);
#5355=ORIENTED_EDGE('',*,*,#3968,.T.);
#5356=ORIENTED_EDGE('',*,*,#3969,.T.);
#5357=ORIENTED_EDGE('',*,*,#3970,.T.);
#5358=ORIENTED_EDGE('',*,*,#3971,.T.);
#5359=ORIENTED_EDGE('',*,*,#3972,.T.);
#5360=ORIENTED_EDGE('',*,*,#3973,.T.);
#5361=ORIENTED_EDGE('',*,*,#3974,.F.);
#5362=ORIENTED_EDGE('',*,*,#3975,.F.);
#5363=ORIENTED_EDGE('',*,*,#3976,.F.);
#5364=ORIENTED_EDGE('',*,*,#3977,.F.);
#5365=ORIENTED_EDGE('',*,*,#3978,.F.);
#5366=ORIENTED_EDGE('',*,*,#3979,.F.);
#5367=ORIENTED_EDGE('',*,*,#3980,.F.);
#5368=ORIENTED_EDGE('',*,*,#3975,.T.);
#5369=ORIENTED_EDGE('',*,*,#3981,.T.);
#5370=ORIENTED_EDGE('',*,*,#3972,.F.);
#5371=ORIENTED_EDGE('',*,*,#3982,.F.);
#5372=ORIENTED_EDGE('',*,*,#3976,.T.);
#5373=ORIENTED_EDGE('',*,*,#3982,.T.);
#5374=ORIENTED_EDGE('',*,*,#3971,.F.);
#5375=ORIENTED_EDGE('',*,*,#3983,.F.);
#5376=ORIENTED_EDGE('',*,*,#3977,.T.);
#5377=ORIENTED_EDGE('',*,*,#3983,.T.);
#5378=ORIENTED_EDGE('',*,*,#3970,.F.);
#5379=ORIENTED_EDGE('',*,*,#3984,.F.);
#5380=ORIENTED_EDGE('',*,*,#3978,.T.);
#5381=ORIENTED_EDGE('',*,*,#3984,.T.);
#5382=ORIENTED_EDGE('',*,*,#3969,.F.);
#5383=ORIENTED_EDGE('',*,*,#3985,.F.);
#5384=ORIENTED_EDGE('',*,*,#3979,.T.);
#5385=ORIENTED_EDGE('',*,*,#3985,.T.);
#5386=ORIENTED_EDGE('',*,*,#3968,.F.);
#5387=ORIENTED_EDGE('',*,*,#3986,.F.);
#5388=ORIENTED_EDGE('',*,*,#3974,.T.);
#5389=ORIENTED_EDGE('',*,*,#3986,.T.);
#5390=ORIENTED_EDGE('',*,*,#3967,.F.);
#5391=ORIENTED_EDGE('',*,*,#3981,.F.);
#5392=ORIENTED_EDGE('',*,*,#3987,.F.);
#5393=ORIENTED_EDGE('',*,*,#3965,.T.);
#5394=ORIENTED_EDGE('',*,*,#3987,.T.);
#5395=ORIENTED_EDGE('',*,*,#3988,.T.);
#5396=ORIENTED_EDGE('',*,*,#3989,.F.);
#5397=ORIENTED_EDGE('',*,*,#3988,.F.);
#5398=ORIENTED_EDGE('',*,*,#3990,.F.);
#5399=ORIENTED_EDGE('',*,*,#3989,.T.);
#5400=ORIENTED_EDGE('',*,*,#3973,.F.);
#5401=ORIENTED_EDGE('',*,*,#3991,.T.);
#5402=ORIENTED_EDGE('',*,*,#3990,.T.);
#5403=ORIENTED_EDGE('',*,*,#3991,.F.);
#5404=ORIENTED_EDGE('',*,*,#3992,.F.);
#5405=ORIENTED_EDGE('',*,*,#3993,.T.);
#5406=ORIENTED_EDGE('',*,*,#3980,.T.);
#5407=ORIENTED_EDGE('',*,*,#3993,.F.);
#5408=ORIENTED_EDGE('',*,*,#3992,.T.);
#5409=ORIENTED_EDGE('',*,*,#3994,.F.);
#5410=ORIENTED_EDGE('',*,*,#3994,.T.);
#5411=ORIENTED_EDGE('',*,*,#3995,.T.);
#5412=ORIENTED_EDGE('',*,*,#3966,.T.);
#5413=ORIENTED_EDGE('',*,*,#3995,.F.);
#5682=CYLINDRICAL_SURFACE('',#7119,0.43);
#5683=CYLINDRICAL_SURFACE('',#7136,0.46);
#5684=CYLINDRICAL_SURFACE('',#7140,0.525);
#5685=CYLINDRICAL_SURFACE('',#7141,0.515);
#5686=CYLINDRICAL_SURFACE('',#7145,0.2);
#6012=ADVANCED_FACE('',(#1113),#5682,.F.);
#6013=ADVANCED_FACE('',(#1114,#556),#760,.T.);
#6014=ADVANCED_FACE('',(#1115,#557),#761,.T.);
#6015=ADVANCED_FACE('',(#1116,#558),#762,.F.);
#6016=ADVANCED_FACE('',(#1117),#763,.T.);
#6017=ADVANCED_FACE('',(#1118),#764,.T.);
#6018=ADVANCED_FACE('',(#1119),#765,.T.);
#6019=ADVANCED_FACE('',(#1120),#766,.T.);
#6020=ADVANCED_FACE('',(#1121),#767,.T.);
#6021=ADVANCED_FACE('',(#1122),#768,.T.);
#6022=ADVANCED_FACE('',(#1123,#559),#769,.T.);
#6023=ADVANCED_FACE('',(#1124),#5683,.F.);
#6024=ADVANCED_FACE('',(#1125,#560),#770,.T.);
#6025=ADVANCED_FACE('',(#1126),#5684,.T.);
#6026=ADVANCED_FACE('',(#1127),#5685,.T.);
#6027=ADVANCED_FACE('',(#1128,#561),#771,.T.);
#6028=ADVANCED_FACE('',(#1129),#5686,.F.);
#6100=CLOSED_SHELL('',(#6012,#6013,#6014,#6015,#6016,#6017,#6018,#6019,
#6020,#6021,#6022,#6023,#6024,#6025,#6026,#6027,#6028));
#7118=AXIS2_PLACEMENT_3D('',#11073,#8837,#8838);
#7119=AXIS2_PLACEMENT_3D('',#11074,#8839,#8840);
#7120=AXIS2_PLACEMENT_3D('',#11076,#8841,#8842);
#7121=AXIS2_PLACEMENT_3D('',#11079,#8844,#8845);
#7122=AXIS2_PLACEMENT_3D('',#11080,#8846,#8847);
#7123=AXIS2_PLACEMENT_3D('',#11082,#8848,#8849);
#7124=AXIS2_PLACEMENT_3D('',#11083,#8850,#8851);
#7125=AXIS2_PLACEMENT_3D('',#11097,#8858,#8859);
#7126=AXIS2_PLACEMENT_3D('',#11098,#8860,#8861);
#7127=AXIS2_PLACEMENT_3D('',#11112,#8868,#8869);
#7128=AXIS2_PLACEMENT_3D('',#11113,#8870,#8871);
#7129=AXIS2_PLACEMENT_3D('',#11116,#8874,#8875);
#7130=AXIS2_PLACEMENT_3D('',#11118,#8877,#8878);
#7131=AXIS2_PLACEMENT_3D('',#11120,#8880,#8881);
#7132=AXIS2_PLACEMENT_3D('',#11122,#8883,#8884);
#7133=AXIS2_PLACEMENT_3D('',#11124,#8886,#8887);
#7134=AXIS2_PLACEMENT_3D('',#11125,#8888,#8889);
#7135=AXIS2_PLACEMENT_3D('',#11127,#8890,#8891);
#7136=AXIS2_PLACEMENT_3D('',#11128,#8892,#8893);
#7137=AXIS2_PLACEMENT_3D('',#11131,#8895,#8896);
#7138=AXIS2_PLACEMENT_3D('',#11132,#8897,#8898);
#7139=AXIS2_PLACEMENT_3D('',#11134,#8899,#8900);
#7140=AXIS2_PLACEMENT_3D('',#11135,#8901,#8902);
#7141=AXIS2_PLACEMENT_3D('',#11137,#8904,#8905);
#7142=AXIS2_PLACEMENT_3D('',#11139,#8906,#8907);
#7143=AXIS2_PLACEMENT_3D('',#11141,#8909,#8910);
#7144=AXIS2_PLACEMENT_3D('',#11143,#8911,#8912);
#7145=AXIS2_PLACEMENT_3D('',#11144,#8913,#8914);
#8837=DIRECTION('axis',(0.,0.,1.));
#8838=DIRECTION('refdir',(1.,0.,0.));
#8839=DIRECTION('center_axis',(0.,1.,0.));
#8840=DIRECTION('ref_axis',(1.,0.,0.));
#8841=DIRECTION('center_axis',(0.,1.,0.));
#8842=DIRECTION('ref_axis',(1.,0.,0.));
#8843=DIRECTION('',(0.,1.,0.));
#8844=DIRECTION('center_axis',(0.,-1.,0.));
#8845=DIRECTION('ref_axis',(1.,0.,0.));
#8846=DIRECTION('center_axis',(0.,1.,0.));
#8847=DIRECTION('ref_axis',(1.,0.,0.));
#8848=DIRECTION('center_axis',(0.,1.,0.));
#8849=DIRECTION('ref_axis',(1.,0.,0.));
#8850=DIRECTION('center_axis',(0.,1.,0.));
#8851=DIRECTION('ref_axis',(1.,0.,0.));
#8852=DIRECTION('',(0.5,0.,-0.866025403784439));
#8853=DIRECTION('',(-0.5,0.,-0.866025403784439));
#8854=DIRECTION('',(-1.,0.,-1.60246890531964E-16));
#8855=DIRECTION('',(-0.5,0.,0.866025403784439));
#8856=DIRECTION('',(0.5,0.,0.866025403784439));
#8857=DIRECTION('',(1.,0.,1.60246890531964E-16));
#8858=DIRECTION('center_axis',(0.,-1.,0.));
#8859=DIRECTION('ref_axis',(1.,0.,0.));
#8860=DIRECTION('center_axis',(0.,1.,0.));
#8861=DIRECTION('ref_axis',(1.,0.,0.));
#8862=DIRECTION('',(0.5,0.,-0.866025403784439));
#8863=DIRECTION('',(1.,0.,1.60246890531964E-16));
#8864=DIRECTION('',(0.5,0.,0.866025403784439));
#8865=DIRECTION('',(-0.5,0.,0.866025403784439));
#8866=DIRECTION('',(-1.,0.,-1.60246890531964E-16));
#8867=DIRECTION('',(-0.5,0.,-0.866025403784439));
#8868=DIRECTION('center_axis',(0.,-1.,0.));
#8869=DIRECTION('ref_axis',(1.,0.,0.));
#8870=DIRECTION('center_axis',(-1.60246890531964E-16,0.,1.));
#8871=DIRECTION('ref_axis',(1.,0.,1.60246890531964E-16));
#8872=DIRECTION('',(0.,1.,0.));
#8873=DIRECTION('',(0.,1.,0.));
#8874=DIRECTION('center_axis',(-0.866025403784439,0.,0.5));
#8875=DIRECTION('ref_axis',(0.5,0.,0.866025403784439));
#8876=DIRECTION('',(0.,1.,0.));
#8877=DIRECTION('center_axis',(-0.866025403784439,0.,-0.5));
#8878=DIRECTION('ref_axis',(-0.5,0.,0.866025403784439));
#8879=DIRECTION('',(0.,1.,0.));
#8880=DIRECTION('center_axis',(1.60246890531964E-16,0.,-1.));
#8881=DIRECTION('ref_axis',(-1.,0.,-1.60246890531964E-16));
#8882=DIRECTION('',(0.,1.,0.));
#8883=DIRECTION('center_axis',(0.866025403784439,0.,-0.5));
#8884=DIRECTION('ref_axis',(-0.5,0.,-0.866025403784439));
#8885=DIRECTION('',(0.,1.,0.));
#8886=DIRECTION('center_axis',(0.866025403784439,0.,0.5));
#8887=DIRECTION('ref_axis',(0.5,0.,-0.866025403784439));
#8888=DIRECTION('center_axis',(0.,1.,0.));
#8889=DIRECTION('ref_axis',(0.,0.,1.));
#8890=DIRECTION('center_axis',(0.,-1.,0.));
#8891=DIRECTION('ref_axis',(1.,0.,0.));
#8892=DIRECTION('center_axis',(0.,-1.,0.));
#8893=DIRECTION('ref_axis',(1.,0.,0.));
#8894=DIRECTION('',(0.,1.,0.));
#8895=DIRECTION('center_axis',(0.,-1.,0.));
#8896=DIRECTION('ref_axis',(1.,0.,0.));
#8897=DIRECTION('center_axis',(0.,1.,0.));
#8898=DIRECTION('ref_axis',(0.,0.,1.));
#8899=DIRECTION('center_axis',(0.,-1.,0.));
#8900=DIRECTION('ref_axis',(1.,0.,0.));
#8901=DIRECTION('center_axis',(0.,-1.,0.));
#8902=DIRECTION('ref_axis',(1.,0.,0.));
#8903=DIRECTION('',(0.,1.,0.));
#8904=DIRECTION('center_axis',(0.,-1.,0.));
#8905=DIRECTION('ref_axis',(1.,0.,0.));
#8906=DIRECTION('center_axis',(0.,-1.,0.));
#8907=DIRECTION('ref_axis',(1.,0.,0.));
#8908=DIRECTION('',(0.,1.,0.));
#8909=DIRECTION('center_axis',(0.,-1.,0.));
#8910=DIRECTION('ref_axis',(0.,0.,-1.));
#8911=DIRECTION('center_axis',(0.,-1.,0.));
#8912=DIRECTION('ref_axis',(1.,0.,0.));
#8913=DIRECTION('center_axis',(0.,-1.,0.));
#8914=DIRECTION('ref_axis',(1.,0.,0.));
#8915=DIRECTION('',(0.,1.,0.));
#11073=CARTESIAN_POINT('',(0.,0.,0.));
#11074=CARTESIAN_POINT('Origin',(0.,0.6,0.));
#11075=CARTESIAN_POINT('',(-0.43,0.6,5.26598123633362E-17));
#11076=CARTESIAN_POINT('Origin',(0.,0.6,0.));
#11077=CARTESIAN_POINT('',(-0.43,0.7,-5.26598123633362E-17));
#11078=CARTESIAN_POINT('',(-0.43,0.6,5.26598123633362E-17));
#11079=CARTESIAN_POINT('Origin',(0.,0.7,0.));
#11080=CARTESIAN_POINT('Origin',(0.,0.6,0.));
#11081=CARTESIAN_POINT('',(-0.2,0.6,2.44929359829471E-17));
#11082=CARTESIAN_POINT('Origin',(0.,0.6,0.));
#11083=CARTESIAN_POINT('Origin',(0.,0.5,-1.11022302462516E-16));
#11084=CARTESIAN_POINT('',(0.346410161513776,0.5,0.6));
#11085=CARTESIAN_POINT('',(0.692820323027551,0.5,0.));
#11086=CARTESIAN_POINT('',(0.346410161513776,0.5,0.6));
#11087=CARTESIAN_POINT('',(0.346410161513776,0.5,-0.6));
#11088=CARTESIAN_POINT('',(0.692820323027551,0.5,0.));
#11089=CARTESIAN_POINT('',(-0.346410161513775,0.5,-0.6));
#11090=CARTESIAN_POINT('',(0.346410161513776,0.5,-0.6));
#11091=CARTESIAN_POINT('',(-0.692820323027551,0.5,-8.48460190979926E-17));
#11092=CARTESIAN_POINT('',(-0.346410161513775,0.5,-0.6));
#11093=CARTESIAN_POINT('',(-0.346410161513776,0.5,0.6));
#11094=CARTESIAN_POINT('',(-0.692820323027551,0.5,-8.48460190979926E-17));
#11095=CARTESIAN_POINT('',(-0.346410161513776,0.5,0.6));
#11096=CARTESIAN_POINT('',(-0.525,0.5,-6.4293956955236E-17));
#11097=CARTESIAN_POINT('Origin',(0.,0.5,0.));
#11098=CARTESIAN_POINT('Origin',(0.,0.,-1.11022302462516E-16));
#11099=CARTESIAN_POINT('',(0.346410161513776,0.,0.6));
#11100=CARTESIAN_POINT('',(0.692820323027551,0.,0.));
#11101=CARTESIAN_POINT('',(0.346410161513776,0.,0.6));
#11102=CARTESIAN_POINT('',(-0.346410161513776,0.,0.6));
#11103=CARTESIAN_POINT('',(-0.346410161513776,0.,0.6));
#11104=CARTESIAN_POINT('',(-0.692820323027551,0.,-8.48460190979926E-17));
#11105=CARTESIAN_POINT('',(-0.692820323027551,0.,-8.48460190979926E-17));
#11106=CARTESIAN_POINT('',(-0.346410161513775,0.,-0.6));
#11107=CARTESIAN_POINT('',(-0.346410161513775,0.,-0.6));
#11108=CARTESIAN_POINT('',(0.346410161513776,0.,-0.6));
#11109=CARTESIAN_POINT('',(0.346410161513776,0.,-0.6));
#11110=CARTESIAN_POINT('',(0.692820323027551,0.,0.));
#11111=CARTESIAN_POINT('',(-0.515,0.,-6.30693101560887E-17));
#11112=CARTESIAN_POINT('Origin',(0.,0.,0.));
#11113=CARTESIAN_POINT('Origin',(-0.346410161513776,0.,0.6));
#11114=CARTESIAN_POINT('',(0.346410161513776,0.,0.6));
#11115=CARTESIAN_POINT('',(-0.346410161513776,0.,0.6));
#11116=CARTESIAN_POINT('Origin',(-0.692820323027551,0.,-8.48460190979926E-17));
#11117=CARTESIAN_POINT('',(-0.692820323027551,0.,-8.48460190979926E-17));
#11118=CARTESIAN_POINT('Origin',(-0.346410161513775,0.,-0.6));
#11119=CARTESIAN_POINT('',(-0.346410161513775,0.,-0.6));
#11120=CARTESIAN_POINT('Origin',(0.346410161513776,0.,-0.6));
#11121=CARTESIAN_POINT('',(0.346410161513776,0.,-0.6));
#11122=CARTESIAN_POINT('Origin',(0.692820323027551,0.,0.));
#11123=CARTESIAN_POINT('',(0.692820323027551,0.,0.));
#11124=CARTESIAN_POINT('Origin',(0.346410161513776,0.,0.6));
#11125=CARTESIAN_POINT('Origin',(0.46,0.7,0.));
#11126=CARTESIAN_POINT('',(-0.46,0.7,-5.63337527607782E-17));
#11127=CARTESIAN_POINT('Origin',(0.,0.7,0.));
#11128=CARTESIAN_POINT('Origin',(0.,1.2,0.));
#11129=CARTESIAN_POINT('',(-0.46,1.7,-5.63337527607782E-17));
#11130=CARTESIAN_POINT('',(-0.46,1.2,-5.63337527607782E-17));
#11131=CARTESIAN_POINT('Origin',(0.,1.7,0.));
#11132=CARTESIAN_POINT('Origin',(0.525,1.7,0.));
#11133=CARTESIAN_POINT('',(-0.525,1.7,-6.4293956955236E-17));
#11134=CARTESIAN_POINT('Origin',(0.,1.7,0.));
#11135=CARTESIAN_POINT('Origin',(0.,1.1,0.));
#11136=CARTESIAN_POINT('',(-0.525,1.1,-6.4293956955236E-17));
#11137=CARTESIAN_POINT('Origin',(0.,-0.325,0.));
#11138=CARTESIAN_POINT('',(-0.515,-0.65,-6.30693101560887E-17));
#11139=CARTESIAN_POINT('Origin',(0.,-0.65,0.));
#11140=CARTESIAN_POINT('',(-0.515,-0.325,-6.30693101560887E-17));
#11141=CARTESIAN_POINT('Origin',(0.2,-0.65,0.));
#11142=CARTESIAN_POINT('',(-0.2,-0.65,-2.44929359829471E-17));
#11143=CARTESIAN_POINT('Origin',(0.,-0.65,0.));
#11144=CARTESIAN_POINT('Origin',(0.,0.0249999999999999,0.));
#11145=CARTESIAN_POINT('',(-0.2,0.0249999999999999,-2.44929359829471E-17));
#11389=UNCERTAINTY_MEASURE_WITH_UNIT(LENGTH_MEASURE(0.001),#11433,
'DISTANCE_ACCURACY_VALUE',
'Maximum model space distance between geometric entities at asserted c
onnectivities');
#11393=UNCERTAINTY_MEASURE_WITH_UNIT(LENGTH_MEASURE(0.001),#11433,
'DISTANCE_ACCURACY_VALUE',
'Maximum model space distance between geometric entities at asserted c
onnectivities');
#11428=(
GEOMETRIC_REPRESENTATION_CONTEXT(3)
GLOBAL_UNCERTAINTY_ASSIGNED_CONTEXT((#11389))
GLOBAL_UNIT_ASSIGNED_CONTEXT((#11433,#11435,#11436))
REPRESENTATION_CONTEXT('','3D')
);
#11432=(
GEOMETRIC_REPRESENTATION_CONTEXT(3)
GLOBAL_UNCERTAINTY_ASSIGNED_CONTEXT((#11393))
GLOBAL_UNIT_ASSIGNED_CONTEXT((#11433,#11435,#11436))
REPRESENTATION_CONTEXT('','3D')
);
#11433=(
LENGTH_UNIT()
NAMED_UNIT(*)
SI_UNIT(.CENTI.,.METRE.)
);
#11435=(
NAMED_UNIT(*)
PLANE_ANGLE_UNIT()
SI_UNIT($,.RADIAN.)
);
#11436=(
NAMED_UNIT(*)
SI_UNIT($,.STERADIAN.)
SOLID_ANGLE_UNIT()
);
#11471=SHAPE_DEFINITION_REPRESENTATION(#11509,#11597);
#11509=PRODUCT_DEFINITION_SHAPE('',$,#11636);
#11597=SHAPE_REPRESENTATION('',(#7118),#11428);
#11601=PRODUCT_DEFINITION_CONTEXT('part definition',#11717,'design');
#11636=PRODUCT_DEFINITION('Body','Body',#11674,#11601);
#11674=PRODUCT_DEFINITION_FORMATION('',$,#11753);
#11717=APPLICATION_CONTEXT(
'Core Data for Automotive Mechanical Design Process');
#11718=PRODUCT_CONTEXT('part definition',#11717,'mechanical');
#11753=PRODUCT('Body','Body','Body',(#11718));
#11792=COLOUR_RGB('Dark Blue',0.08,0.2,0.34);
#11793=FILL_AREA_STYLE_COLOUR('',#11792);
#11794=FILL_AREA_STYLE('',(#11793));
#11795=SURFACE_STYLE_FILL_AREA(#11794);
#11796=SURFACE_SIDE_STYLE('',(#11795));
#11797=SURFACE_STYLE_USAGE(.BOTH.,#11796);
#11798=PRESENTATION_STYLE_ASSIGNMENT((#11797));
ENDSEC;
END-ISO-10303-21;
